ISO-10303-21;
HEADER;
FILE_DESCRIPTION (('STEP AP214'),
    '1' );
FILE_NAME ('roller axis assy_r5.step',
    '2026-10-24T11:01:53',
    ( '' ),
    ( '' ),
    'SwSTEP 2.0',
    'SolidWorks 2026',
    '' );
FILE_SCHEMA (( 'AUTOMOTIVE_DESIGN' ));
ENDSEC;

DATA;
#36=LINE ( 'NONE', #1308, #2826 ) ;
#51=EDGE_LOOP ( 'NONE', ( #1765, #1748 ) ) ;
#59=CARTESIAN_POINT ( 'NONE',  ( 5.000000000000000000, -5.000000000000000000, 7.000000000000006217 ) ) ;
#62=LINE ( 'NONE', #7469, #2279 ) ;
#77=LINE ( 'NONE', #5562, #6140 ) ;
#100=DIRECTION ( 'NONE',  ( 0.000000000000000000, 0.000000000000000000, -1.000000000000000000 ) ) ;
#130=LINE ( 'NONE', #5451, #8061 ) ;
#160=CIRCLE ( 'NONE', #1848, 10.00000000000000000 ) ;
#176=VECTOR ( 'NONE', #5079, 1000.000000000000000 ) ;
#184=ORIENTED_EDGE ( 'NONE', *, *, #1602, .F. ) ;
#207=CARTESIAN_POINT ( 'NONE',  ( 10.00000000000000000, 0.000000000000000000, 140.0000000000000000 ) ) ;
#231=CARTESIAN_POINT ( 'NONE',  ( -5.000000000000000000, -5.000000000000000000, -0.9999999999999940048 ) ) ;
#258=DIRECTION ( 'NONE',  ( -0.000000000000000000, 0.000000000000000000, 1.000000000000000000 ) ) ;
#260=ORIENTED_EDGE ( 'NONE', *, *, #2345, .F. ) ;
#304=CARTESIAN_POINT ( 'NONE',  ( 0.000000000000000000, 0.000000000000000000, 7.000000000000006217 ) ) ;
#319=ORIENTED_EDGE ( 'NONE', *, *, #4563, .T. ) ;
#323=ORIENTED_EDGE ( 'NONE', *, *, #2666, .F. ) ;
#332=FACE_BOUND ( 'NONE', #3831, .T. ) ;
#345=DIRECTION ( 'NONE',  ( 0.000000000000000000, 1.000000000000000000, 0.000000000000000000 ) ) ;
#367=AXIS2_PLACEMENT_3D ( 'NONE', #5408, #1407, #4068 ) ;
#371=ORIENTED_EDGE ( 'NONE', *, *, #7980, .T. ) ;
#415=ORIENTED_EDGE ( 'NONE', *, *, #2060, .F. ) ;
#425=EDGE_LOOP ( 'NONE', ( #5519, #4503, #7362, #1544 ) ) ;
#435=CARTESIAN_POINT ( 'NONE',  ( 0.000000000000000000, 0.000000000000000000, 7.000000000000006217 ) ) ;
#464=DIRECTION ( 'NONE',  ( 0.000000000000000000, 0.000000000000000000, 1.000000000000000000 ) ) ;
#480=ADVANCED_FACE ( 'NONE', ( #7780 ), #3861, .T. ) ;
#496=CARTESIAN_POINT ( 'NONE',  ( -5.000000000000001776, 5.000000000000001776, -0.9999999999999940048 ) ) ;
#497=CIRCLE ( 'NONE', #1612, 10.00000000000000000 ) ;
#561=PLANE ( 'NONE',  #4523 ) ;
#565=EDGE_LOOP ( 'NONE', ( #768, #2358, #3387, #1842 ) ) ;
#570=DIRECTION ( 'NONE',  ( -0.000000000000000000, -0.000000000000000000, -1.000000000000000000 ) ) ;
#594=AXIS2_PLACEMENT_3D ( 'NONE', #3123, #464, #5764 ) ;
#598=AXIS2_PLACEMENT_3D ( 'NONE', #5344, #7214, #4044 ) ;
#600=SHAPE_DEFINITION_REPRESENTATION ( #5299, #7686 ) ;
#631=ORIENTED_EDGE ( 'NONE', *, *, #5473, .T. ) ;
#646=ORIENTED_EDGE ( 'NONE', *, *, #3675, .F. ) ;
#654=PRODUCT ( 'roller axis assy_r5', 'roller axis assy_r5', '', ( #7013 ) ) ;
#659=CARTESIAN_POINT ( 'NONE',  ( 5.000000000000000000, -5.000000000000000000, 7.000000000000006217 ) ) ;
#674=AXIS2_PLACEMENT_3D ( 'NONE', #6837, #7536, #1532 ) ;
#711=DIRECTION ( 'NONE',  ( -0.000000000000000000, -0.000000000000000000, 1.000000000000000000 ) ) ;
#744=DIRECTION ( 'NONE',  ( -1.734723475976806848E-16, 1.000000000000000000, 0.000000000000000000 ) ) ;
#752=FACE_OUTER_BOUND ( 'NONE', #3034, .T. ) ;
#766=ORIENTED_EDGE ( 'NONE', *, *, #850, .F. ) ;
#768=ORIENTED_EDGE ( 'NONE', *, *, #1199, .F. ) ;
#776=EDGE_CURVE ( 'NONE', #1841, #8324, #2475, .T. ) ;
#806=VERTEX_POINT ( 'NONE', #6265 ) ;
#822=DIRECTION ( 'NONE',  ( 0.000000000000000000, 0.000000000000000000, 1.000000000000000000 ) ) ;
#823=EDGE_CURVE ( 'NONE', #1959, #4658, #1487, .T. ) ;
#845=CYLINDRICAL_SURFACE ( 'NONE', #8071, 20.00000000000000000 ) ;
#850=EDGE_CURVE ( 'NONE', #3060, #1959, #5615, .T. ) ;
#853=ADVANCED_FACE ( 'NONE', ( #3012 ), #2366, .F. ) ;
#858=CARTESIAN_POINT ( 'NONE',  ( 5.000000000000000000, -5.000000000000000000, -0.9999999999999940048 ) ) ;
#863=VERTEX_POINT ( 'NONE', #858 ) ;
#864=DIRECTION ( 'NONE',  ( -1.000000000000000000, 0.000000000000000000, 0.000000000000000000 ) ) ;
#900=ADVANCED_FACE ( 'NONE', ( #8155 ), #4838, .F. ) ;
#919=AXIS2_PLACEMENT_3D ( 'NONE', #4469, #2522, #7750 ) ;
#948=ADVANCED_FACE ( 'NONE', ( #4443 ), #561, .F. ) ;
#950=FACE_OUTER_BOUND ( 'NONE', #3769, .T. ) ;
#953=EDGE_CURVE ( 'NONE', #7048, #8019, #4248, .T. ) ;
#958=VERTEX_POINT ( 'NONE', #1835 ) ;
#1002=CARTESIAN_POINT ( 'NONE',  ( -5.000000000000000000, -5.000000000000000000, 140.0000000000000000 ) ) ;
#1009=VERTEX_POINT ( 'NONE', #3878 ) ;
#1028=DIRECTION ( 'NONE',  ( -1.000000000000000000, 0.000000000000000000, -0.000000000000000000 ) ) ;
#1029=PLANE ( 'NONE',  #4496 ) ;
#1040=CARTESIAN_POINT ( 'NONE',  ( -5.000000000000000000, -5.000000000000000000, 148.0000000000000284 ) ) ;
#1046=DIRECTION ( 'NONE',  ( 0.000000000000000000, 1.000000000000000000, 0.000000000000000000 ) ) ;
#1049=EDGE_LOOP ( 'NONE', ( #7724, #3053, #1355, #2617 ) ) ;
#1068=FACE_OUTER_BOUND ( 'NONE', #2118, .T. ) ;
#1096=AXIS2_PLACEMENT_3D ( 'NONE', #304, #5616, #6747 ) ;
#1113=CIRCLE ( 'NONE', #5961, 10.00000000000000000 ) ;
#1117=VERTEX_POINT ( 'NONE', #3352 ) ;
#1135=DIRECTION ( 'NONE',  ( -1.000000000000000000, 0.000000000000000000, 0.000000000000000000 ) ) ;
#1136=MECHANICAL_DESIGN_GEOMETRIC_PRESENTATION_REPRESENTATION('',(#3632),#5713);
#1143=CIRCLE ( 'NONE', #1708, 10.00000000000000000 ) ;
#1172=VECTOR ( 'NONE', #3157, 1000.000000000000000 ) ;
#1191=AXIS2_PLACEMENT_3D ( 'NONE', #5725, #6385, #8316 ) ;
#1199=EDGE_CURVE ( 'NONE', #2303, #806, #497, .T. ) ;
#1245=CARTESIAN_POINT ( 'NONE',  ( -5.000000000000000000, -5.000000000000000000, 148.0000000000000284 ) ) ;
#1255=LINE ( 'NONE', #7967, #2443 ) ;
#1265=LINE ( 'NONE', #3928, #5668 ) ;
#1267=CARTESIAN_POINT ( 'NONE',  ( 10.00000000000000000, 0.000000000000000000, 120.0000000000000142 ) ) ;
#1272=AXIS2_PLACEMENT_3D ( 'NONE', #496, #1855, #2511 ) ;
#1282=DIRECTION ( 'NONE',  ( -0.000000000000000000, -0.000000000000000000, 1.000000000000000000 ) ) ;
#1296=AXIS2_PLACEMENT_3D ( 'NONE', #1245, #4547, #6634 ) ;
#1308=CARTESIAN_POINT ( 'NONE',  ( 20.00000000000000000, 0.000000000000000000, -49.56854249492377562 ) ) ;
#1329=CLOSED_SHELL ( 'NONE', ( #2505, #7115, #8212, #480, #7684, #1352, #4698, #853, #2558, #1683, #6351, #7379, #3398, #3268, #2324, #900, #7472, #948, #5899, #2633 ) ) ;
#1352=ADVANCED_FACE ( 'NONE', ( #4429 ), #1696, .F. ) ;
#1355=ORIENTED_EDGE ( 'NONE', *, *, #776, .T. ) ;
#1356=LINE ( 'NONE', #3320, #6389 ) ;
#1407=DIRECTION ( 'NONE',  ( -0.000000000000000000, -0.000000000000000000, 1.000000000000000000 ) ) ;
#1408=( GEOMETRIC_REPRESENTATION_CONTEXT ( 3 ) GLOBAL_UNCERTAINTY_ASSIGNED_CONTEXT ( ( #3074 ) ) GLOBAL_UNIT_ASSIGNED_CONTEXT ( ( #3269, #4564, #7927 ) ) REPRESENTATION_CONTEXT ( 'NONE', 'WORKASPACE' ) );
#1420=AXIS2_PLACEMENT_3D ( 'NONE', #2139, #4833, #5521 ) ;
#1461=ORIENTED_EDGE ( 'NONE', *, *, #850, .T. ) ;
#1487=LINE ( 'NONE', #6920, #5368 ) ;
#1489=PLANE ( 'NONE',  #4705 ) ;
#1500=ORIENTED_EDGE ( 'NONE', *, *, #5284, .F. ) ;
#1504=EDGE_CURVE ( 'NONE', #8019, #7048, #6892, .T. ) ;
#1532=DIRECTION ( 'NONE',  ( -1.000000000000000000, 0.000000000000000000, 0.000000000000000000 ) ) ;
#1544=ORIENTED_EDGE ( 'NONE', *, *, #6214, .T. ) ;
#1556=VERTEX_POINT ( 'NONE', #59 ) ;
#1567=DIRECTION ( 'NONE',  ( -1.734723475976806848E-16, 1.000000000000000000, 0.000000000000000000 ) ) ;
#1579=FACE_OUTER_BOUND ( 'NONE', #2274, .T. ) ;
#1602=EDGE_CURVE ( 'NONE', #1117, #6335, #4774, .T. ) ;
#1604=EDGE_LOOP ( 'NONE', ( #4242, #1678 ) ) ;
#1607=DIRECTION ( 'NONE',  ( 0.000000000000000000, 0.000000000000000000, -1.000000000000000000 ) ) ;
#1610=LINE ( 'NONE', #7529, #2126 ) ;
#1612=AXIS2_PLACEMENT_3D ( 'NONE', #6869, #1607, #7617 ) ;
#1630=DIRECTION ( 'NONE',  ( 0.000000000000000000, 0.000000000000000000, 1.000000000000000000 ) ) ;
#1641=CARTESIAN_POINT ( 'NONE',  ( -10.00000000000000000, 1.224646799147353256E-15, 140.0000000000000000 ) ) ;
#1670=ORIENTED_EDGE ( 'NONE', *, *, #3587, .T. ) ;
#1678=ORIENTED_EDGE ( 'NONE', *, *, #953, .T. ) ;
#1683=ADVANCED_FACE ( 'NONE', ( #8092 ), #3509, .T. ) ;
#1693=CARTESIAN_POINT ( 'NONE',  ( -5.000000000000001776, 5.000000000000001776, 148.0000000000000284 ) ) ;
#1696=PLANE ( 'NONE',  #919 ) ;
#1700=PRODUCT_DEFINITION_FORMATION_WITH_SPECIFIED_SOURCE ( 'ANY', '', #654, .NOT_KNOWN. ) ;
#1702=CARTESIAN_POINT ( 'NONE',  ( 5.000000000000000000, -5.000000000000000000, 140.0000000000000000 ) ) ;
#1704=ORIENTED_EDGE ( 'NONE', *, *, #5473, .F. ) ;
#1706=LINE ( 'NONE', #7178, #5061 ) ;
#1708=AXIS2_PLACEMENT_3D ( 'NONE', #6598, #4514, #7170 ) ;
#1748=ORIENTED_EDGE ( 'NONE', *, *, #5809, .F. ) ;
#1765=ORIENTED_EDGE ( 'NONE', *, *, #5595, .F. ) ;
#1773=VECTOR ( 'NONE', #4574, 1000.000000000000000 ) ;
#1810=EDGE_CURVE ( 'NONE', #5548, #3060, #8348, .T. ) ;
#1813=LINE ( 'NONE', #3981, #1172 ) ;
#1835=CARTESIAN_POINT ( 'NONE',  ( -5.000000000000001776, 5.000000000000001776, 140.0000000000000000 ) ) ;
#1841=VERTEX_POINT ( 'NONE', #1641 ) ;
#1842=ORIENTED_EDGE ( 'NONE', *, *, #6954, .F. ) ;
#1848=AXIS2_PLACEMENT_3D ( 'NONE', #7412, #2195, #2886 ) ;
#1855=DIRECTION ( 'NONE',  ( -1.734723475976806848E-16, -1.000000000000000000, 0.000000000000000000 ) ) ;
#1870=FACE_OUTER_BOUND ( 'NONE', #4290, .T. ) ;
#1959=VERTEX_POINT ( 'NONE', #7859 ) ;
#1986=MANIFOLD_SOLID_BREP ( 'Boss-Extrude4', #1329 ) ;
#1990=DIRECTION ( 'NONE',  ( 0.000000000000000000, 0.000000000000000000, 1.000000000000000000 ) ) ;
#2001=ORIENTED_EDGE ( 'NONE', *, *, #2128, .T. ) ;
#2017=PLANE ( 'NONE',  #2348 ) ;
#2018=ORIENTED_EDGE ( 'NONE', *, *, #4563, .F. ) ;
#2028=( LENGTH_UNIT ( ) NAMED_UNIT ( * ) SI_UNIT ( .MILLI., .METRE. ) );
#2060=EDGE_CURVE ( 'NONE', #2610, #7663, #5783, .T. ) ;
#2064=ORIENTED_EDGE ( 'NONE', *, *, #7333, .F. ) ;
#2098=CARTESIAN_POINT ( 'NONE',  ( -5.000000000000001776, 5.000000000000001776, 148.0000000000000284 ) ) ;
#2115=ORIENTED_EDGE ( 'NONE', *, *, #6954, .T. ) ;
#2118=EDGE_LOOP ( 'NONE', ( #319, #2269 ) ) ;
#2126=VECTOR ( 'NONE', #1567, 1000.000000000000000 ) ;
#2128=EDGE_CURVE ( 'NONE', #5009, #3592, #3111, .T. ) ;
#2139=CARTESIAN_POINT ( 'NONE',  ( 0.000000000000000000, 0.000000000000000000, 7.000000000000006217 ) ) ;
#2146=CYLINDRICAL_SURFACE ( 'NONE', #1096, 10.00000000000000000 ) ;
#2195=DIRECTION ( 'NONE',  ( 0.000000000000000000, 0.000000000000000000, -1.000000000000000000 ) ) ;
#2210=EDGE_CURVE ( 'NONE', #863, #3178, #6618, .T. ) ;
#2222=SURFACE_SIDE_STYLE ('',( #3442 ) ) ;
#2230=DIRECTION ( 'NONE',  ( -1.734723475976806848E-16, 1.000000000000000000, 0.000000000000000000 ) ) ;
#2269=ORIENTED_EDGE ( 'NONE', *, *, #1199, .T. ) ;
#2274=EDGE_LOOP ( 'NONE', ( #4630, #7257, #2639, #7405 ) ) ;
#2279=VECTOR ( 'NONE', #6025, 1000.000000000000000 ) ;
#2303=VERTEX_POINT ( 'NONE', #5226 ) ;
#2317=PRESENTATION_STYLE_ASSIGNMENT (( #3611 ) ) ;
#2320=ORIENTED_EDGE ( 'NONE', *, *, #5595, .T. ) ;
#2324=ADVANCED_FACE ( 'NONE', ( #752 ), #2017, .F. ) ;
#2325=VECTOR ( 'NONE', #5417, 1000.000000000000000 ) ;
#2340=ORIENTED_EDGE ( 'NONE', *, *, #8248, .T. ) ;
#2345=EDGE_CURVE ( 'NONE', #1959, #5488, #1265, .T. ) ;
#2348=AXIS2_PLACEMENT_3D ( 'NONE', #2098, #7274, #4571 ) ;
#2355=CARTESIAN_POINT ( 'NONE',  ( -5.000000000000000000, -5.000000000000000000, 140.0000000000000000 ) ) ;
#2358=ORIENTED_EDGE ( 'NONE', *, *, #6509, .T. ) ;
#2360=LINE ( 'NONE', #1702, #5318 ) ;
#2366=PLANE ( 'NONE',  #4409 ) ;
#2387=DIRECTION ( 'NONE',  ( -1.000000000000000000, 0.000000000000000000, -0.000000000000000000 ) ) ;
#2406=VERTEX_POINT ( 'NONE', #5876 ) ;
#2413=CARTESIAN_POINT ( 'NONE',  ( 0.000000000000000000, 0.000000000000000000, 120.0000000000000142 ) ) ;
#2433=DIRECTION ( 'NONE',  ( -1.000000000000000000, 1.734723475976806848E-16, -0.000000000000000000 ) ) ;
#2441=EDGE_LOOP ( 'NONE', ( #5332, #8168 ) ) ;
#2443=VECTOR ( 'NONE', #2576, 1000.000000000000000 ) ;
#2456=CYLINDRICAL_SURFACE ( 'NONE', #6925, 10.00000000000000000 ) ;
#2475=CIRCLE ( 'NONE', #8167, 10.00000000000000000 ) ;
#2476=ORIENTED_EDGE ( 'NONE', *, *, #953, .F. ) ;
#2505=ADVANCED_FACE ( 'NONE', ( #5529 ), #2146, .T. ) ;
#2511=DIRECTION ( 'NONE',  ( 1.000000000000000000, -1.734723475976806848E-16, 0.000000000000000000 ) ) ;
#2520=CARTESIAN_POINT ( 'NONE',  ( 5.000000000000000000, -5.000000000000000000, -0.9999999999999940048 ) ) ;
#2522=DIRECTION ( 'NONE',  ( 1.000000000000000000, 1.734723475976806848E-16, 0.000000000000000000 ) ) ;
#2534=EDGE_CURVE ( 'NONE', #7663, #2610, #4846, .T. ) ;
#2535=DIRECTION ( 'NONE',  ( 0.000000000000000000, 0.000000000000000000, 1.000000000000000000 ) ) ;
#2558=ADVANCED_FACE ( 'NONE', ( #1579 ), #1489, .F. ) ;
#2571=PRODUCT_DEFINITION ( 'UNKNOWN', '', #1700, #2643 ) ;
#2576=DIRECTION ( 'NONE',  ( -0.000000000000000000, -0.000000000000000000, 1.000000000000000000 ) ) ;
#2610=VERTEX_POINT ( 'NONE', #6921 ) ;
#2617=ORIENTED_EDGE ( 'NONE', *, *, #3587, .F. ) ;
#2625=AXIS2_PLACEMENT_3D ( 'NONE', #7416, #7992, #7456 ) ;
#2633=ADVANCED_FACE ( 'NONE', ( #7628 ), #2456, .T. ) ;
#2639=ORIENTED_EDGE ( 'NONE', *, *, #2210, .F. ) ;
#2643=PRODUCT_DEFINITION_CONTEXT ( 'detailed design', #5240, 'design' ) ;
#2662=DIRECTION ( 'NONE',  ( -1.000000000000000000, 0.000000000000000000, 0.000000000000000000 ) ) ;
#2666=EDGE_CURVE ( 'NONE', #6335, #1556, #8419, .T. ) ;
#2706=ORIENTED_EDGE ( 'NONE', *, *, #7980, .F. ) ;
#2710=AXIS2_PLACEMENT_3D ( 'NONE', #7479, #822, #5516 ) ;
#2718=DIRECTION ( 'NONE',  ( 1.734723475976806848E-16, -1.000000000000000000, -0.000000000000000000 ) ) ;
#2746=ORIENTED_EDGE ( 'NONE', *, *, #6509, .F. ) ;
#2749=ORIENTED_EDGE ( 'NONE', *, *, #4020, .T. ) ;
#2789=ORIENTED_EDGE ( 'NONE', *, *, #4020, .F. ) ;
#2794=DIRECTION ( 'NONE',  ( 0.000000000000000000, 1.000000000000000000, 0.000000000000000000 ) ) ;
#2826=VECTOR ( 'NONE', #7314, 1000.000000000000000 ) ;
#2852=ORIENTED_EDGE ( 'NONE', *, *, #6007, .F. ) ;
#2878=AXIS2_PLACEMENT_3D ( 'NONE', #4423, #1282, #8401 ) ;
#2879=DIRECTION ( 'NONE',  ( 1.000000000000000000, 1.734723475976806848E-16, -0.000000000000000000 ) ) ;
#2886=DIRECTION ( 'NONE',  ( -1.000000000000000000, 0.000000000000000000, 0.000000000000000000 ) ) ;
#2890=EDGE_LOOP ( 'NONE', ( #7846, #260, #766, #7376 ) ) ;
#2910=VECTOR ( 'NONE', #7322, 1000.000000000000000 ) ;
#2957=( LENGTH_UNIT ( ) NAMED_UNIT ( * ) SI_UNIT ( .MILLI., .METRE. ) );
#2965=CIRCLE ( 'NONE', #598, 10.00000000000000000 ) ;
#2970=ORIENTED_EDGE ( 'NONE', *, *, #8328, .F. ) ;
#2974=VECTOR ( 'NONE', #2433, 1000.000000000000000 ) ;
#3012=FACE_OUTER_BOUND ( 'NONE', #7621, .T. ) ;
#3034=EDGE_LOOP ( 'NONE', ( #5617, #6860, #3842, #4962 ) ) ;
#3053=ORIENTED_EDGE ( 'NONE', *, *, #3222, .T. ) ;
#3060=VERTEX_POINT ( 'NONE', #6501 ) ;
#3061=EDGE_LOOP ( 'NONE', ( #2746, #2018, #2115, #2320 ) ) ;
#3072=FACE_BOUND ( 'NONE', #51, .T. ) ;
#3074=UNCERTAINTY_MEASURE_WITH_UNIT (LENGTH_MEASURE( 1.000000000000000082E-05 ), #3269, 'distance_accuracy_value', 'NONE');
#3110=CARTESIAN_POINT ( 'NONE',  ( -10.00000000000000000, 1.224646799147353256E-15, 27.00000000000000711 ) ) ;
#3111=LINE ( 'NONE', #4935, #5919 ) ;
#3123=CARTESIAN_POINT ( 'NONE',  ( 0.000000000000000000, 0.000000000000000000, 0.000000000000000000 ) ) ;
#3132=ORIENTED_EDGE ( 'NONE', *, *, #5250, .T. ) ;
#3138=DIRECTION ( 'NONE',  ( 1.734723475976806848E-16, -1.000000000000000000, -0.000000000000000000 ) ) ;
#3157=DIRECTION ( 'NONE',  ( -0.000000000000000000, -0.000000000000000000, 1.000000000000000000 ) ) ;
#3171=FACE_BOUND ( 'NONE', #8408, .T. ) ;
#3178=VERTEX_POINT ( 'NONE', #4716 ) ;
#3222=EDGE_CURVE ( 'NONE', #1009, #1841, #130, .T. ) ;
#3268=ADVANCED_FACE ( 'NONE', ( #6626 ), #5321, .F. ) ;
#3269=( LENGTH_UNIT ( ) NAMED_UNIT ( * ) SI_UNIT ( .MILLI., .METRE. ) );
#3270=VERTEX_POINT ( 'NONE', #4025 ) ;
#3293=STYLED_ITEM('',(#8678),#1986);
#3320=CARTESIAN_POINT ( 'NONE',  ( 5.000000000000000000, -5.000000000000000000, 148.0000000000000284 ) ) ;
#3335=EDGE_LOOP ( 'NONE', ( #4009, #4834, #1670, #7132 ) ) ;
#3351=CARTESIAN_POINT ( 'NONE',  ( -20.00000000000000000, 2.449293598294706513E-15, 120.0000000000000142 ) ) ;
#3352=CARTESIAN_POINT ( 'NONE',  ( -5.000000000000001776, 5.000000000000001776, 7.000000000000006217 ) ) ;
#3381=CARTESIAN_POINT ( 'NONE',  ( 0.000000000000000000, 0.000000000000000000, 120.0000000000000142 ) ) ;
#3383=VECTOR ( 'NONE', #5122, 1000.000000000000000 ) ;
#3387=ORIENTED_EDGE ( 'NONE', *, *, #5809, .T. ) ;
#3398=ADVANCED_FACE ( 'NONE', ( #6234 ), #845, .T. ) ;
#3442=SURFACE_STYLE_FILL_AREA ( #6783 ) ;
#3448=CARTESIAN_POINT ( 'NONE',  ( 5.000000000000000000, -5.000000000000000000, -0.9999999999999940048 ) ) ;
#3481=VECTOR ( 'NONE', #1630, 1000.000000000000000 ) ;
#3486=CYLINDRICAL_SURFACE ( 'NONE', #1420, 10.00000000000000000 ) ;
#3500=DIRECTION ( 'NONE',  ( 0.000000000000000000, 0.000000000000000000, 1.000000000000000000 ) ) ;
#3508=VERTEX_POINT ( 'NONE', #3110 ) ;
#3509=PLANE ( 'NONE',  #4812 ) ;
#3510=VECTOR ( 'NONE', #2718, 1000.000000000000000 ) ;
#3527=FILL_AREA_STYLE_COLOUR ( '', #4599 ) ;
#3570=( NAMED_UNIT ( * ) SI_UNIT ( $, .STERADIAN. ) SOLID_ANGLE_UNIT ( ) );
#3587=EDGE_CURVE ( 'NONE', #3640, #8324, #4659, .T. ) ;
#3592=VERTEX_POINT ( 'NONE', #6004 ) ;
#3611=SURFACE_STYLE_USAGE ( .BOTH. , #2222 ) ;
#3632=STYLED_ITEM ( 'NONE', ( #2317 ), #3979 ) ;
#3640=VERTEX_POINT ( 'NONE', #1267 ) ;
#3671=CARTESIAN_POINT ( 'NONE',  ( 5.000000000000000000, -5.000000000000000000, 140.0000000000000000 ) ) ;
#3675=EDGE_CURVE ( 'NONE', #3060, #8171, #1356, .T. ) ;
#3679=ORIENTED_EDGE ( 'NONE', *, *, #8572, .F. ) ;
#3683=CARTESIAN_POINT ( 'NONE',  ( 0.000000000000000000, 0.000000000000000000, 7.000000000000006217 ) ) ;
#3685=DIRECTION ( 'NONE',  ( 1.000000000000000000, 0.000000000000000000, 0.000000000000000000 ) ) ;
#3717=DIRECTION ( 'NONE',  ( 1.000000000000000000, -1.734723475976806848E-16, 0.000000000000000000 ) ) ;
#3736=EDGE_LOOP ( 'NONE', ( #6828, #2001, #3875, #5931 ) ) ;
#3742=CARTESIAN_POINT ( 'NONE',  ( 5.000000000000000000, 5.000000000000000000, 140.0000000000000000 ) ) ;
#3749=ORIENTED_EDGE ( 'NONE', *, *, #823, .T. ) ;
#3769=EDGE_LOOP ( 'NONE', ( #7771, #6587, #4466, #6991 ) ) ;
#3791=DIRECTION ( 'NONE',  ( 0.000000000000000000, 0.000000000000000000, 1.000000000000000000 ) ) ;
#3804=CARTESIAN_POINT ( 'NONE',  ( 0.000000000000000000, 0.000000000000000000, 120.0000000000000142 ) ) ;
#3831=EDGE_LOOP ( 'NONE', ( #7563, #2064, #1704, #6067 ) ) ;
#3842=ORIENTED_EDGE ( 'NONE', *, *, #823, .F. ) ;
#3850=CARTESIAN_POINT ( 'NONE',  ( 5.000000000000000000, -5.000000000000000000, -0.9999999999999940048 ) ) ;
#3861=CYLINDRICAL_SURFACE ( 'NONE', #2878, 10.00000000000000000 ) ;
#3875=ORIENTED_EDGE ( 'NONE', *, *, #8572, .T. ) ;
#3878=CARTESIAN_POINT ( 'NONE',  ( -10.00000000000000000, 1.224646799147353256E-15, 120.0000000000000142 ) ) ;
#3883=ORIENTED_EDGE ( 'NONE', *, *, #7246, .T. ) ;
#3917=APPLICATION_CONTEXT ( 'automotive_design' ) ;
#3928=CARTESIAN_POINT ( 'NONE',  ( 5.000000000000000000, 5.000000000000000000, 148.0000000000000284 ) ) ;
#3979=ADVANCED_BREP_SHAPE_REPRESENTATION ( '', ( #1986, #594 ), #1408 ) ;
#3981=CARTESIAN_POINT ( 'NONE',  ( -10.00000000000000000, 1.224646799147353256E-15, 7.000000000000006217 ) ) ;
#3992=EDGE_LOOP ( 'NONE', ( #1461, #3749, #371, #6989 ) ) ;
#3994=PLANE ( 'NONE',  #1296 ) ;
#4009=ORIENTED_EDGE ( 'NONE', *, *, #3222, .F. ) ;
#4017=DIRECTION ( 'NONE',  ( -0.000000000000000000, -0.000000000000000000, -1.000000000000000000 ) ) ;
#4020=EDGE_CURVE ( 'NONE', #7663, #7048, #5494, .T. ) ;
#4025=CARTESIAN_POINT ( 'NONE',  ( -5.000000000000000000, -5.000000000000000000, 7.000000000000006217 ) ) ;
#4043=ORIENTED_EDGE ( 'NONE', *, *, #1504, .F. ) ;
#4044=DIRECTION ( 'NONE',  ( -1.000000000000000000, 0.000000000000000000, 0.000000000000000000 ) ) ;
#4068=DIRECTION ( 'NONE',  ( -1.000000000000000000, 0.000000000000000000, 0.000000000000000000 ) ) ;
#4127=DIRECTION ( 'NONE',  ( 0.000000000000000000, 0.000000000000000000, -1.000000000000000000 ) ) ;
#4180=DIRECTION ( 'NONE',  ( -1.000000000000000000, 0.000000000000000000, -0.000000000000000000 ) ) ;
#4201=DIRECTION ( 'NONE',  ( -1.000000000000000000, 0.000000000000000000, -0.000000000000000000 ) ) ;
#4210=VECTOR ( 'NONE', #2662, 1000.000000000000000 ) ;
#4242=ORIENTED_EDGE ( 'NONE', *, *, #1504, .T. ) ;
#4248=CIRCLE ( 'NONE', #6745, 20.00000000000000000 ) ;
#4261=EDGE_CURVE ( 'NONE', #3640, #1009, #1113, .T. ) ;
#4290=EDGE_LOOP ( 'NONE', ( #4385, #646, #4422, #3883 ) ) ;
#4329=PLANE ( 'NONE',  #8538 ) ;
#4353=DIRECTION ( 'NONE',  ( -0.000000000000000000, -0.000000000000000000, 1.000000000000000000 ) ) ;
#4380=CARTESIAN_POINT ( 'NONE',  ( -5.000000000000000000, -5.000000000000000000, 148.0000000000000284 ) ) ;
#4385=ORIENTED_EDGE ( 'NONE', *, *, #7333, .T. ) ;
#4386=PLANE ( 'NONE',  #1191 ) ;
#4409=AXIS2_PLACEMENT_3D ( 'NONE', #5007, #4180, #258 ) ;
#4422=ORIENTED_EDGE ( 'NONE', *, *, #1810, .F. ) ;
#4423=CARTESIAN_POINT ( 'NONE',  ( 0.000000000000000000, 0.000000000000000000, 7.000000000000006217 ) ) ;
#4429=FACE_OUTER_BOUND ( 'NONE', #425, .T. ) ;
#4443=FACE_OUTER_BOUND ( 'NONE', #2890, .T. ) ;
#4461=EDGE_CURVE ( 'NONE', #8171, #5488, #2360, .T. ) ;
#4466=ORIENTED_EDGE ( 'NONE', *, *, #2128, .F. ) ;
#4469=CARTESIAN_POINT ( 'NONE',  ( -5.000000000000000000, -5.000000000000000000, -0.9999999999999940048 ) ) ;
#4496=AXIS2_PLACEMENT_3D ( 'NONE', #3683, #5676, #2387 ) ;
#4502=VECTOR ( 'NONE', #5373, 1000.000000000000000 ) ;
#4503=ORIENTED_EDGE ( 'NONE', *, *, #6775, .F. ) ;
#4514=DIRECTION ( 'NONE',  ( 0.000000000000000000, 0.000000000000000000, -1.000000000000000000 ) ) ;
#4523=AXIS2_PLACEMENT_3D ( 'NONE', #7009, #1135, #2535 ) ;
#4547=DIRECTION ( 'NONE',  ( 0.000000000000000000, 1.000000000000000000, 0.000000000000000000 ) ) ;
#4563=EDGE_CURVE ( 'NONE', #806, #2303, #1143, .T. ) ;
#4564=( NAMED_UNIT ( * ) PLANE_ANGLE_UNIT ( ) SI_UNIT ( $, .RADIAN. ) );
#4571=DIRECTION ( 'NONE',  ( 1.000000000000000000, -1.734723475976806848E-16, 0.000000000000000000 ) ) ;
#4574=DIRECTION ( 'NONE',  ( -1.000000000000000000, 0.000000000000000000, 0.000000000000000000 ) ) ;
#4599=COLOUR_RGB ( '',0.8941176470588234615, 0.8941176470588234615, 0.8941176470588234615 ) ;
#4630=ORIENTED_EDGE ( 'NONE', *, *, #5284, .T. ) ;
#4658=VERTEX_POINT ( 'NONE', #6681 ) ;
#4659=LINE ( 'NONE', #6049, #2910 ) ;
#4698=ADVANCED_FACE ( 'NONE', ( #950 ), #4904, .F. ) ;
#4705=AXIS2_PLACEMENT_3D ( 'NONE', #3448, #2794, #8117 ) ;
#4716=CARTESIAN_POINT ( 'NONE',  ( -5.000000000000000000, -5.000000000000000000, -0.9999999999999940048 ) ) ;
#4719=EDGE_LOOP ( 'NONE', ( #631, #8043, #2706, #6105 ) ) ;
#4767=CIRCLE ( 'NONE', #5311, 10.00000000000000000 ) ;
#4774=LINE ( 'NONE', #7512, #2325 ) ;
#4803=( NAMED_UNIT ( * ) PLANE_ANGLE_UNIT ( ) SI_UNIT ( $, .RADIAN. ) );
#4812=AXIS2_PLACEMENT_3D ( 'NONE', #6066, #100, #4201 ) ;
#4824=VECTOR ( 'NONE', #345, 1000.000000000000000 ) ;
#4833=DIRECTION ( 'NONE',  ( -0.000000000000000000, -0.000000000000000000, 1.000000000000000000 ) ) ;
#4834=ORIENTED_EDGE ( 'NONE', *, *, #8543, .T. ) ;
#4838=PLANE ( 'NONE',  #8033 ) ;
#4846=CIRCLE ( 'NONE', #674, 20.00000000000000000 ) ;
#4884=CARTESIAN_POINT ( 'NONE',  ( -5.000000000000001776, 5.000000000000001776, -0.9999999999999940048 ) ) ;
#4889=CARTESIAN_POINT ( 'NONE',  ( 0.000000000000000000, 0.000000000000000000, -49.56854249492377562 ) ) ;
#4904=PLANE ( 'NONE',  #1272 ) ;
#4926=DIRECTION ( 'NONE',  ( 0.000000000000000000, 0.000000000000000000, -1.000000000000000000 ) ) ;
#4935=CARTESIAN_POINT ( 'NONE',  ( -5.000000000000001776, 5.000000000000001776, -0.9999999999999940048 ) ) ;
#4953=CYLINDRICAL_SURFACE ( 'NONE', #2710, 20.00000000000000000 ) ;
#4962=ORIENTED_EDGE ( 'NONE', *, *, #2345, .T. ) ;
#4966=DIRECTION ( 'NONE',  ( -1.000000000000000000, 0.000000000000000000, 0.000000000000000000 ) ) ;
#4983=FACE_OUTER_BOUND ( 'NONE', #6957, .T. ) ;
#5007=CARTESIAN_POINT ( 'NONE',  ( 5.000000000000000000, 5.000000000000000000, -0.9999999999999940048 ) ) ;
#5008=DIRECTION ( 'NONE',  ( -0.000000000000000000, -0.000000000000000000, 1.000000000000000000 ) ) ;
#5009=VERTEX_POINT ( 'NONE', #4884 ) ;
#5061=VECTOR ( 'NONE', #4353, 1000.000000000000000 ) ;
#5079=DIRECTION ( 'NONE',  ( -0.000000000000000000, -0.000000000000000000, -1.000000000000000000 ) ) ;
#5088=CARTESIAN_POINT ( 'NONE',  ( -5.000000000000000000, -5.000000000000000000, 148.0000000000000284 ) ) ;
#5122=DIRECTION ( 'NONE',  ( -0.000000000000000000, -0.000000000000000000, -1.000000000000000000 ) ) ;
#5226=CARTESIAN_POINT ( 'NONE',  ( -10.00000000000000000, 1.224646799147353256E-15, 7.000000000000006217 ) ) ;
#5240=APPLICATION_CONTEXT ( 'automotive_design' ) ;
#5242=DIRECTION ( 'NONE',  ( 1.000000000000000000, 0.000000000000000000, -0.000000000000000000 ) ) ;
#5250=EDGE_CURVE ( 'NONE', #2610, #8019, #36, .T. ) ;
#5284=EDGE_CURVE ( 'NONE', #1556, #3270, #7222, .T. ) ;
#5299=PRODUCT_DEFINITION_SHAPE ( 'NONE', 'NONE',  #2571 ) ;
#5311=AXIS2_PLACEMENT_3D ( 'NONE', #6166, #4127, #864 ) ;
#5318=VECTOR ( 'NONE', #1046, 1000.000000000000000 ) ;
#5321=PLANE ( 'NONE',  #2625 ) ;
#5324=ORIENTED_EDGE ( 'NONE', *, *, #4261, .F. ) ;
#5332=ORIENTED_EDGE ( 'NONE', *, *, #8064, .F. ) ;
#5340=ORIENTED_EDGE ( 'NONE', *, *, #2534, .T. ) ;
#5344=CARTESIAN_POINT ( 'NONE',  ( 0.000000000000000000, 0.000000000000000000, 27.00000000000000711 ) ) ;
#5367=( NAMED_UNIT ( * ) SI_UNIT ( $, .STERADIAN. ) SOLID_ANGLE_UNIT ( ) );
#5368=VECTOR ( 'NONE', #8329, 1000.000000000000000 ) ;
#5373=DIRECTION ( 'NONE',  ( -0.000000000000000000, -0.000000000000000000, 1.000000000000000000 ) ) ;
#5408=CARTESIAN_POINT ( 'NONE',  ( 0.000000000000000000, 0.000000000000000000, 27.00000000000001066 ) ) ;
#5417=DIRECTION ( 'NONE',  ( 1.000000000000000000, -1.734723475976806848E-16, 0.000000000000000000 ) ) ;
#5451=CARTESIAN_POINT ( 'NONE',  ( -10.00000000000000000, 1.224646799147353256E-15, 7.000000000000006217 ) ) ;
#5463=CARTESIAN_POINT ( 'NONE',  ( 0.000000000000000000, 0.000000000000000000, 120.0000000000000142 ) ) ;
#5473=EDGE_CURVE ( 'NONE', #958, #5730, #7624, .T. ) ;
#5480=SHAPE_REPRESENTATION_RELATIONSHIP ( 'NONE' , 'NONE' ,  #7686, #3979 ) ;
#5481=DIRECTION ( 'NONE',  ( -0.000000000000000000, -0.000000000000000000, 1.000000000000000000 ) ) ;
#5488=VERTEX_POINT ( 'NONE', #3742 ) ;
#5494=LINE ( 'NONE', #6927, #3481 ) ;
#5508=DIRECTION ( 'NONE',  ( 1.000000000000000000, 0.000000000000000000, 0.000000000000000000 ) ) ;
#5516=DIRECTION ( 'NONE',  ( 1.000000000000000000, 0.000000000000000000, 0.000000000000000000 ) ) ;
#5519=ORIENTED_EDGE ( 'NONE', *, *, #8328, .T. ) ;
#5521=DIRECTION ( 'NONE',  ( 1.000000000000000000, 0.000000000000000000, 0.000000000000000000 ) ) ;
#5529=FACE_OUTER_BOUND ( 'NONE', #1049, .T. ) ;
#5535=CARTESIAN_POINT ( 'NONE',  ( -5.000000000000000000, -5.000000000000000000, 148.0000000000000284 ) ) ;
#5548=VERTEX_POINT ( 'NONE', #5088 ) ;
#5562=CARTESIAN_POINT ( 'NONE',  ( 5.000000000000000000, 5.000000000000000000, -0.9999999999999940048 ) ) ;
#5595=EDGE_CURVE ( 'NONE', #2406, #3508, #2965, .T. ) ;
#5599=AXIS2_PLACEMENT_3D ( 'NONE', #3381, #1990, #5242 ) ;
#5615=LINE ( 'NONE', #6312, #4824 ) ;
#5616=DIRECTION ( 'NONE',  ( -0.000000000000000000, -0.000000000000000000, 1.000000000000000000 ) ) ;
#5617=ORIENTED_EDGE ( 'NONE', *, *, #7749, .T. ) ;
#5668=VECTOR ( 'NONE', #570, 1000.000000000000000 ) ;
#5676=DIRECTION ( 'NONE',  ( 0.000000000000000000, 0.000000000000000000, -1.000000000000000000 ) ) ;
#5687=LINE ( 'NONE', #1693, #3383 ) ;
#5695=EDGE_LOOP ( 'NONE', ( #6731, #2749, #4043, #7386 ) ) ;
#5700=DIRECTION ( 'NONE',  ( 1.000000000000000000, 0.000000000000000000, 0.000000000000000000 ) ) ;
#5713=( GEOMETRIC_REPRESENTATION_CONTEXT ( 3 ) GLOBAL_UNCERTAINTY_ASSIGNED_CONTEXT ( ( #8390 ) ) GLOBAL_UNIT_ASSIGNED_CONTEXT ( ( #2957, #6825, #3570 ) ) REPRESENTATION_CONTEXT ( 'NONE', 'WORKASPACE' ) );
#5725=CARTESIAN_POINT ( 'NONE',  ( 0.000000000000000000, 0.000000000000000000, 140.0000000000000000 ) ) ;
#5730=VERTEX_POINT ( 'NONE', #7350 ) ;
#5742=VECTOR ( 'NONE', #7038, 1000.000000000000000 ) ;
#5764=DIRECTION ( 'NONE',  ( 1.000000000000000000, 0.000000000000000000, 0.000000000000000000 ) ) ;
#5783=CIRCLE ( 'NONE', #367, 20.00000000000000000 ) ;
#5809=EDGE_CURVE ( 'NONE', #3508, #2406, #4767, .T. ) ;
#5846=PLANE ( 'NONE',  #5599 ) ;
#5869=CIRCLE ( 'NONE', #8522, 10.00000000000000000 ) ;
#5876=CARTESIAN_POINT ( 'NONE',  ( 10.00000000000000000, 0.000000000000000000, 27.00000000000000711 ) ) ;
#5899=ADVANCED_FACE ( 'NONE', ( #8405, #332 ), #4386, .F. ) ;
#5919=VECTOR ( 'NONE', #3717, 1000.000000000000000 ) ;
#5931=ORIENTED_EDGE ( 'NONE', *, *, #2210, .T. ) ;
#5936=CARTESIAN_POINT ( 'NONE',  ( 0.000000000000000000, 0.000000000000000000, 120.0000000000000142 ) ) ;
#5961=AXIS2_PLACEMENT_3D ( 'NONE', #3804, #7809, #8503 ) ;
#6004=CARTESIAN_POINT ( 'NONE',  ( 5.000000000000000000, 5.000000000000000000, -0.9999999999999940048 ) ) ;
#6007=EDGE_CURVE ( 'NONE', #863, #1556, #7907, .T. ) ;
#6018=LINE ( 'NONE', #231, #4502 ) ;
#6025=DIRECTION ( 'NONE',  ( 0.000000000000000000, -1.000000000000000000, 0.000000000000000000 ) ) ;
#6049=CARTESIAN_POINT ( 'NONE',  ( 10.00000000000000000, 0.000000000000000000, 7.000000000000006217 ) ) ;
#6053=LINE ( 'NONE', #5535, #3510 ) ;
#6066=CARTESIAN_POINT ( 'NONE',  ( 0.000000000000000000, 0.000000000000000000, -0.9999999999999940048 ) ) ;
#6067=ORIENTED_EDGE ( 'NONE', *, *, #7749, .F. ) ;
#6105=ORIENTED_EDGE ( 'NONE', *, *, #7281, .T. ) ;
#6122=FACE_OUTER_BOUND ( 'NONE', #565, .T. ) ;
#6140=VECTOR ( 'NONE', #5481, 1000.000000000000000 ) ;
#6160=DIRECTION ( 'NONE',  ( 0.000000000000000000, 0.000000000000000000, 1.000000000000000000 ) ) ;
#6164=EDGE_LOOP ( 'NONE', ( #2970, #1500, #323, #184 ) ) ;
#6166=CARTESIAN_POINT ( 'NONE',  ( 0.000000000000000000, 0.000000000000000000, 27.00000000000000711 ) ) ;
#6174=CARTESIAN_POINT ( 'NONE',  ( -5.000000000000000000, -5.000000000000000000, -0.9999999999999940048 ) ) ;
#6179=CARTESIAN_POINT ( 'NONE',  ( -5.000000000000000000, -5.000000000000000000, 148.0000000000000284 ) ) ;
#6214=EDGE_CURVE ( 'NONE', #3178, #3270, #6018, .T. ) ;
#6234=FACE_OUTER_BOUND ( 'NONE', #6247, .T. ) ;
#6245=ORIENTED_EDGE ( 'NONE', *, *, #2534, .F. ) ;
#6247=EDGE_LOOP ( 'NONE', ( #2789, #5340, #3132, #2476 ) ) ;
#6265=CARTESIAN_POINT ( 'NONE',  ( 10.00000000000000000, 0.000000000000000000, 7.000000000000006217 ) ) ;
#6298=LINE ( 'NONE', #2355, #5742 ) ;
#6312=CARTESIAN_POINT ( 'NONE',  ( 5.000000000000000000, -5.000000000000000000, 148.0000000000000284 ) ) ;
#6322=DIRECTION ( 'NONE',  ( 1.000000000000000000, 0.000000000000000000, 0.000000000000000000 ) ) ;
#6335=VERTEX_POINT ( 'NONE', #6935 ) ;
#6351=ADVANCED_FACE ( 'NONE', ( #3072, #4983 ), #4329, .T. ) ;
#6371=CARTESIAN_POINT ( 'NONE',  ( -5.000000000000001776, 5.000000000000001776, 140.0000000000000000 ) ) ;
#6385=DIRECTION ( 'NONE',  ( 0.000000000000000000, 0.000000000000000000, -1.000000000000000000 ) ) ;
#6389=VECTOR ( 'NONE', #4017, 1000.000000000000000 ) ;
#6484=( GEOMETRIC_REPRESENTATION_CONTEXT ( 3 ) GLOBAL_UNCERTAINTY_ASSIGNED_CONTEXT ( ( #8271 ) ) GLOBAL_UNIT_ASSIGNED_CONTEXT ( ( #2028, #4803, #5367 ) ) REPRESENTATION_CONTEXT ( 'NONE', 'WORKASPACE' ) );
#6501=CARTESIAN_POINT ( 'NONE',  ( 5.000000000000000000, -5.000000000000000000, 148.0000000000000284 ) ) ;
#6509=EDGE_CURVE ( 'NONE', #2303, #3508, #1813, .T. ) ;
#6587=ORIENTED_EDGE ( 'NONE', *, *, #8248, .F. ) ;
#6592=VECTOR ( 'NONE', #7202, 1000.000000000000000 ) ;
#6598=CARTESIAN_POINT ( 'NONE',  ( 0.000000000000000000, 0.000000000000000000, 7.000000000000006217 ) ) ;
#6618=LINE ( 'NONE', #3850, #1773 ) ;
#6626=FACE_OUTER_BOUND ( 'NONE', #3992, .T. ) ;
#6634=DIRECTION ( 'NONE',  ( 0.000000000000000000, -0.000000000000000000, 1.000000000000000000 ) ) ;
#6681=CARTESIAN_POINT ( 'NONE',  ( -5.000000000000001776, 5.000000000000001776, 148.0000000000000284 ) ) ;
#6731=ORIENTED_EDGE ( 'NONE', *, *, #2060, .T. ) ;
#6745=AXIS2_PLACEMENT_3D ( 'NONE', #2413, #3791, #7801 ) ;
#6747=DIRECTION ( 'NONE',  ( 1.000000000000000000, 0.000000000000000000, 0.000000000000000000 ) ) ;
#6754=CARTESIAN_POINT ( 'NONE',  ( 20.00000000000000000, 0.000000000000000000, 120.0000000000000142 ) ) ;
#6775=EDGE_CURVE ( 'NONE', #5009, #1117, #1706, .T. ) ;
#6783=FILL_AREA_STYLE ('',( #3527 ) ) ;
#6788=VECTOR ( 'NONE', #7010, 1000.000000000000000 ) ;
#6825=( NAMED_UNIT ( * ) PLANE_ANGLE_UNIT ( ) SI_UNIT ( $, .RADIAN. ) );
#6828=ORIENTED_EDGE ( 'NONE', *, *, #8287, .T. ) ;
#6837=CARTESIAN_POINT ( 'NONE',  ( 0.000000000000000000, 0.000000000000000000, 27.00000000000001066 ) ) ;
#6845=VECTOR ( 'NONE', #744, 1000.000000000000000 ) ;
#6860=ORIENTED_EDGE ( 'NONE', *, *, #7281, .F. ) ;
#6869=CARTESIAN_POINT ( 'NONE',  ( 0.000000000000000000, 0.000000000000000000, 7.000000000000006217 ) ) ;
#6892=CIRCLE ( 'NONE', #8021, 20.00000000000000000 ) ;
#6895=CARTESIAN_POINT ( 'NONE',  ( 0.000000000000000000, 0.000000000000000000, 27.00000000000000711 ) ) ;
#6920=CARTESIAN_POINT ( 'NONE',  ( -5.000000000000001776, 5.000000000000001776, 148.0000000000000284 ) ) ;
#6921=CARTESIAN_POINT ( 'NONE',  ( 20.00000000000000000, 0.000000000000000000, 27.00000000000001066 ) ) ;
#6925=AXIS2_PLACEMENT_3D ( 'NONE', #435, #5008, #5700 ) ;
#6927=CARTESIAN_POINT ( 'NONE',  ( -20.00000000000000000, 2.449293598294706513E-15, -49.56854249492377562 ) ) ;
#6935=CARTESIAN_POINT ( 'NONE',  ( 5.000000000000000000, 5.000000000000000000, 7.000000000000006217 ) ) ;
#6954=EDGE_CURVE ( 'NONE', #806, #2406, #1255, .T. ) ;
#6957=EDGE_LOOP ( 'NONE', ( #415, #6245 ) ) ;
#6964=ORIENTED_EDGE ( 'NONE', *, *, #8543, .F. ) ;
#6978=DIRECTION ( 'NONE',  ( 0.000000000000000000, 0.000000000000000000, -1.000000000000000000 ) ) ;
#6989=ORIENTED_EDGE ( 'NONE', *, *, #1810, .T. ) ;
#6991=ORIENTED_EDGE ( 'NONE', *, *, #6775, .T. ) ;
#7009=CARTESIAN_POINT ( 'NONE',  ( 5.000000000000000000, -5.000000000000000000, 148.0000000000000284 ) ) ;
#7010=DIRECTION ( 'NONE',  ( 0.000000000000000000, -1.000000000000000000, 0.000000000000000000 ) ) ;
#7013=PRODUCT_CONTEXT ( 'NONE', #3917, 'mechanical' ) ;
#7023=ORIENTED_EDGE ( 'NONE', *, *, #2666, .T. ) ;
#7027=FACE_BOUND ( 'NONE', #6164, .T. ) ;
#7038=DIRECTION ( 'NONE',  ( 1.000000000000000000, 0.000000000000000000, 0.000000000000000000 ) ) ;
#7048=VERTEX_POINT ( 'NONE', #3351 ) ;
#7070=CARTESIAN_POINT ( 'NONE',  ( -20.00000000000000000, 2.449293598294706513E-15, 27.00000000000001066 ) ) ;
#7115=ADVANCED_FACE ( 'NONE', ( #7435 ), #4953, .T. ) ;
#7132=ORIENTED_EDGE ( 'NONE', *, *, #8064, .T. ) ;
#7170=DIRECTION ( 'NONE',  ( -1.000000000000000000, 0.000000000000000000, 0.000000000000000000 ) ) ;
#7178=CARTESIAN_POINT ( 'NONE',  ( -5.000000000000001776, 5.000000000000001776, -0.9999999999999940048 ) ) ;
#7202=DIRECTION ( 'NONE',  ( -0.000000000000000000, -0.000000000000000000, 1.000000000000000000 ) ) ;
#7214=DIRECTION ( 'NONE',  ( 0.000000000000000000, 0.000000000000000000, -1.000000000000000000 ) ) ;
#7222=LINE ( 'NONE', #659, #4210 ) ;
#7246=EDGE_CURVE ( 'NONE', #5548, #5730, #8317, .T. ) ;
#7257=ORIENTED_EDGE ( 'NONE', *, *, #6214, .F. ) ;
#7270=VECTOR ( 'NONE', #3138, 1000.000000000000000 ) ;
#7274=DIRECTION ( 'NONE',  ( -1.734723475976806848E-16, -1.000000000000000000, 0.000000000000000000 ) ) ;
#7281=EDGE_CURVE ( 'NONE', #4658, #958, #5687, .T. ) ;
#7295=DIRECTION ( 'NONE',  ( 1.000000000000000000, 0.000000000000000000, 0.000000000000000000 ) ) ;
#7314=DIRECTION ( 'NONE',  ( 0.000000000000000000, 0.000000000000000000, 1.000000000000000000 ) ) ;
#7322=DIRECTION ( 'NONE',  ( -0.000000000000000000, -0.000000000000000000, 1.000000000000000000 ) ) ;
#7333=EDGE_CURVE ( 'NONE', #5730, #8171, #6298, .T. ) ;
#7350=CARTESIAN_POINT ( 'NONE',  ( -5.000000000000000000, -5.000000000000000000, 140.0000000000000000 ) ) ;
#7362=ORIENTED_EDGE ( 'NONE', *, *, #8287, .F. ) ;
#7376=ORIENTED_EDGE ( 'NONE', *, *, #3675, .T. ) ;
#7379=ADVANCED_FACE ( 'NONE', ( #3171, #7864 ), #5846, .T. ) ;
#7386=ORIENTED_EDGE ( 'NONE', *, *, #5250, .F. ) ;
#7396=LINE ( 'NONE', #6174, #6845 ) ;
#7405=ORIENTED_EDGE ( 'NONE', *, *, #6007, .T. ) ;
#7412=CARTESIAN_POINT ( 'NONE',  ( 0.000000000000000000, 0.000000000000000000, 140.0000000000000000 ) ) ;
#7416=CARTESIAN_POINT ( 'NONE',  ( 0.000000000000000000, 0.000000000000000000, 148.0000000000000284 ) ) ;
#7435=FACE_OUTER_BOUND ( 'NONE', #5695, .T. ) ;
#7456=DIRECTION ( 'NONE',  ( -1.000000000000000000, 0.000000000000000000, -0.000000000000000000 ) ) ;
#7469=CARTESIAN_POINT ( 'NONE',  ( 5.000000000000000000, 5.000000000000000000, -0.9999999999999940048 ) ) ;
#7472=ADVANCED_FACE ( 'NONE', ( #1870 ), #3994, .F. ) ;
#7479=CARTESIAN_POINT ( 'NONE',  ( 0.000000000000000000, 0.000000000000000000, -49.56854249492377562 ) ) ;
#7512=CARTESIAN_POINT ( 'NONE',  ( -5.000000000000001776, 5.000000000000001776, 7.000000000000006217 ) ) ;
#7529=CARTESIAN_POINT ( 'NONE',  ( -5.000000000000000000, -5.000000000000000000, 7.000000000000006217 ) ) ;
#7535=CARTESIAN_POINT ( 'NONE',  ( 0.000000000000000000, 0.000000000000000000, 140.0000000000000000 ) ) ;
#7536=DIRECTION ( 'NONE',  ( -0.000000000000000000, -0.000000000000000000, 1.000000000000000000 ) ) ;
#7563=ORIENTED_EDGE ( 'NONE', *, *, #4461, .F. ) ;
#7617=DIRECTION ( 'NONE',  ( -1.000000000000000000, 0.000000000000000000, 0.000000000000000000 ) ) ;
#7621=EDGE_LOOP ( 'NONE', ( #7023, #2852, #3679, #2340 ) ) ;
#7624=LINE ( 'NONE', #1002, #7270 ) ;
#7628=FACE_OUTER_BOUND ( 'NONE', #3335, .T. ) ;
#7663=VERTEX_POINT ( 'NONE', #7070 ) ;
#7684=ADVANCED_FACE ( 'NONE', ( #7027, #1068 ), #1029, .T. ) ;
#7686=SHAPE_REPRESENTATION ( 'roller axis assy_r5', ( #594 ), #1408 ) ;
#7724=ORIENTED_EDGE ( 'NONE', *, *, #4261, .T. ) ;
#7749=EDGE_CURVE ( 'NONE', #5488, #958, #8306, .T. ) ;
#7750=DIRECTION ( 'NONE',  ( -1.734723475976806848E-16, 1.000000000000000000, 0.000000000000000000 ) ) ;
#7771=ORIENTED_EDGE ( 'NONE', *, *, #1602, .T. ) ;
#7780=FACE_OUTER_BOUND ( 'NONE', #3061, .T. ) ;
#7801=DIRECTION ( 'NONE',  ( 1.000000000000000000, 0.000000000000000000, 0.000000000000000000 ) ) ;
#7809=DIRECTION ( 'NONE',  ( 0.000000000000000000, 0.000000000000000000, 1.000000000000000000 ) ) ;
#7846=ORIENTED_EDGE ( 'NONE', *, *, #4461, .T. ) ;
#7859=CARTESIAN_POINT ( 'NONE',  ( 5.000000000000000000, 5.000000000000000000, 148.0000000000000284 ) ) ;
#7864=FACE_OUTER_BOUND ( 'NONE', #1604, .T. ) ;
#7875=VECTOR ( 'NONE', #3685, 1000.000000000000000 ) ;
#7907=LINE ( 'NONE', #2520, #6592 ) ;
#7927=( NAMED_UNIT ( * ) SI_UNIT ( $, .STERADIAN. ) SOLID_ANGLE_UNIT ( ) );
#7967=CARTESIAN_POINT ( 'NONE',  ( 10.00000000000000000, 0.000000000000000000, 7.000000000000006217 ) ) ;
#7980=EDGE_CURVE ( 'NONE', #4658, #5548, #6053, .T. ) ;
#7992=DIRECTION ( 'NONE',  ( 0.000000000000000000, 0.000000000000000000, -1.000000000000000000 ) ) ;
#8019=VERTEX_POINT ( 'NONE', #6754 ) ;
#8021=AXIS2_PLACEMENT_3D ( 'NONE', #5936, #8569, #7295 ) ;
#8033=AXIS2_PLACEMENT_3D ( 'NONE', #6179, #2879, #2230 ) ;
#8043=ORIENTED_EDGE ( 'NONE', *, *, #7246, .F. ) ;
#8061=VECTOR ( 'NONE', #711, 1000.000000000000000 ) ;
#8064=EDGE_CURVE ( 'NONE', #8324, #1841, #160, .T. ) ;
#8071=AXIS2_PLACEMENT_3D ( 'NONE', #4889, #3500, #6322 ) ;
#8092=FACE_OUTER_BOUND ( 'NONE', #3736, .T. ) ;
#8117=DIRECTION ( 'NONE',  ( 0.000000000000000000, -0.000000000000000000, 1.000000000000000000 ) ) ;
#8155=FACE_OUTER_BOUND ( 'NONE', #4719, .T. ) ;
#8167=AXIS2_PLACEMENT_3D ( 'NONE', #7535, #4926, #4966 ) ;
#8168=ORIENTED_EDGE ( 'NONE', *, *, #776, .F. ) ;
#8171=VERTEX_POINT ( 'NONE', #3671 ) ;
#8212=ADVANCED_FACE ( 'NONE', ( #6122 ), #3486, .T. ) ;
#8248=EDGE_CURVE ( 'NONE', #3592, #6335, #77, .T. ) ;
#8271=UNCERTAINTY_MEASURE_WITH_UNIT (LENGTH_MEASURE( 1.000000000000000082E-05 ), #2028, 'distance_accuracy_value', 'NONE');
#8287=EDGE_CURVE ( 'NONE', #3178, #5009, #7396, .T. ) ;
#8306=LINE ( 'NONE', #6371, #2974 ) ;
#8316=DIRECTION ( 'NONE',  ( -1.000000000000000000, 0.000000000000000000, -0.000000000000000000 ) ) ;
#8317=LINE ( 'NONE', #1040, #176 ) ;
#8324=VERTEX_POINT ( 'NONE', #207 ) ;
#8328=EDGE_CURVE ( 'NONE', #3270, #1117, #1610, .T. ) ;
#8329=DIRECTION ( 'NONE',  ( -1.000000000000000000, 1.734723475976806848E-16, -0.000000000000000000 ) ) ;
#8348=LINE ( 'NONE', #4380, #7875 ) ;
#8371=CARTESIAN_POINT ( 'NONE',  ( 5.000000000000000000, 5.000000000000000000, 7.000000000000006217 ) ) ;
#8390=UNCERTAINTY_MEASURE_WITH_UNIT (LENGTH_MEASURE( 1.000000000000000082E-05 ), #2957, 'distance_accuracy_value', 'NONE');
#8401=DIRECTION ( 'NONE',  ( 1.000000000000000000, 0.000000000000000000, 0.000000000000000000 ) ) ;
#8405=FACE_OUTER_BOUND ( 'NONE', #2441, .T. ) ;
#8408=EDGE_LOOP ( 'NONE', ( #5324, #6964 ) ) ;
#8419=LINE ( 'NONE', #8371, #6788 ) ;
#8503=DIRECTION ( 'NONE',  ( 1.000000000000000000, 0.000000000000000000, 0.000000000000000000 ) ) ;
#8522=AXIS2_PLACEMENT_3D ( 'NONE', #5463, #6160, #5508 ) ;
#8538=AXIS2_PLACEMENT_3D ( 'NONE', #6895, #6978, #1028 ) ;
#8543=EDGE_CURVE ( 'NONE', #1009, #3640, #5869, .T. ) ;
#8569=DIRECTION ( 'NONE',  ( 0.000000000000000000, 0.000000000000000000, 1.000000000000000000 ) ) ;
#8572=EDGE_CURVE ( 'NONE', #3592, #863, #62, .T. ) ;
#8580=MECHANICAL_DESIGN_GEOMETRIC_PRESENTATION_REPRESENTATION('',(#3293),#6484);
#8672=COLOUR_RGB('Off White',0.89,0.88,0.83);
#8673=FILL_AREA_STYLE_COLOUR('',#8672);
#8674=FILL_AREA_STYLE('',(#8673));
#8675=SURFACE_STYLE_FILL_AREA(#8674);
#8676=SURFACE_SIDE_STYLE('',(#8675));
#8677=SURFACE_STYLE_USAGE(.BOTH.,#8676);
#8678=PRESENTATION_STYLE_ASSIGNMENT((#8677));
ENDSEC;
END-ISO-10303-21;
